ISO-10303-21;
HEADER;
FILE_DESCRIPTION((''),'2;1');
FILE_NAME('SHELL_CLAMP_NUT_M6.step','2026-10-01T22:05:39-07:00',(''),(''),'','','');
FILE_SCHEMA (('AUTOMOTIVE_DESIGN { 1 0 10303 214 3 1 1 }'));
ENDSEC;
DATA;
#10=MECHANICAL_DESIGN_GEOMETRIC_PRESENTATION_REPRESENTATION('',(#646),#24628);
#562=SHAPE_REPRESENTATION_RELATIONSHIP('SRR','None',#24837,#604) ;
#604=ADVANCED_BREP_SHAPE_REPRESENTATION('',(#685),#24627) ;
#646=STYLED_ITEM('',(#25030),#685) ;
#685=MANIFOLD_SOLID_BREP('SHELL_CLAMP_NUT_M6',#13188) ;
#949=FACE_BOUND('',#4744,.T.) ;
#950=FACE_BOUND('',#4750,.T.) ;
#1818=LINE('',#24470,#2654) ;
#1819=LINE('',#24475,#2655) ;
#1820=LINE('',#24477,#2656) ;
#1821=LINE('',#24479,#2657) ;
#1822=LINE('',#24480,#2658) ;
#1823=LINE('',#24484,#2659) ;
#1824=LINE('',#24486,#2660) ;
#1825=LINE('',#24488,#2661) ;
#1826=LINE('',#24489,#2662) ;
#1827=LINE('',#24492,#2663) ;
#1828=LINE('',#24493,#2664) ;
#1829=LINE('',#24495,#2665) ;
#1830=LINE('',#24496,#2666) ;
#1831=LINE('',#24499,#2667) ;
#1832=LINE('',#24500,#2668) ;
#1833=LINE('',#24503,#2669) ;
#1834=LINE('',#24504,#2670) ;
#1835=LINE('',#24506,#2671) ;
#1836=LINE('',#24508,#2672) ;
#2654=VECTOR('',#19619,0.3) ;
#2655=VECTOR('',#19624,1.) ;
#2656=VECTOR('',#19625,1.) ;
#2657=VECTOR('',#19626,1.) ;
#2658=VECTOR('',#19627,1.) ;
#2659=VECTOR('',#19630,1.) ;
#2660=VECTOR('',#19631,1.) ;
#2661=VECTOR('',#19632,1.) ;
#2662=VECTOR('',#19633,1.) ;
#2663=VECTOR('',#19636,1.) ;
#2664=VECTOR('',#19637,1.) ;
#2665=VECTOR('',#19638,1.) ;
#2666=VECTOR('',#19639,1.) ;
#2667=VECTOR('',#19642,1.) ;
#2668=VECTOR('',#19643,1.) ;
#2669=VECTOR('',#19646,1.) ;
#2670=VECTOR('',#19647,1.) ;
#2671=VECTOR('',#19650,1.) ;
#2672=VECTOR('',#19653,1.) ;
#2951=CYLINDRICAL_SURFACE('',#15356,0.3) ;
#3710=FACE_OUTER_BOUND('',#4740,.T.) ;
#3711=FACE_OUTER_BOUND('',#4741,.T.) ;
#3712=FACE_OUTER_BOUND('',#4742,.T.) ;
#3713=FACE_OUTER_BOUND('',#4743,.T.) ;
#3714=FACE_OUTER_BOUND('',#4745,.T.) ;
#3715=FACE_OUTER_BOUND('',#4746,.T.) ;
#3716=FACE_OUTER_BOUND('',#4747,.T.) ;
#3717=FACE_OUTER_BOUND('',#4748,.T.) ;
#3718=FACE_OUTER_BOUND('',#4749,.T.) ;
#4740=EDGE_LOOP('',(#11953,#11954,#11955,#11956)) ;
#4741=EDGE_LOOP('',(#11957,#11958,#11959,#11960)) ;
#4742=EDGE_LOOP('',(#11961,#11962,#11963,#11964)) ;
#4743=EDGE_LOOP('',(#11965,#11966,#11967,#11968,#11969,#11970)) ;
#4744=EDGE_LOOP('',(#11971)) ;
#4745=EDGE_LOOP('',(#11972,#11973,#11974,#11975)) ;
#4746=EDGE_LOOP('',(#11976,#11977,#11978,#11979)) ;
#4747=EDGE_LOOP('',(#11980,#11981,#11982,#11983)) ;
#4748=EDGE_LOOP('',(#11984,#11985,#11986,#11987)) ;
#4749=EDGE_LOOP('',(#11988,#11989,#11990,#11991,#11992,#11993)) ;
#4750=EDGE_LOOP('',(#11994)) ;
#5535=CIRCLE('',#15357,0.3) ;
#5536=CIRCLE('',#15358,0.3) ;
#6719=VERTEX_POINT('',#24467) ;
#6720=VERTEX_POINT('',#24469) ;
#6721=VERTEX_POINT('',#24473) ;
#6722=VERTEX_POINT('',#24474) ;
#6723=VERTEX_POINT('',#24476) ;
#6724=VERTEX_POINT('',#24478) ;
#6725=VERTEX_POINT('',#24482) ;
#6726=VERTEX_POINT('',#24483) ;
#6727=VERTEX_POINT('',#24485) ;
#6728=VERTEX_POINT('',#24487) ;
#6729=VERTEX_POINT('',#24491) ;
#6730=VERTEX_POINT('',#24494) ;
#6731=VERTEX_POINT('',#24498) ;
#6732=VERTEX_POINT('',#24502) ;
#8466=EDGE_CURVE('',#6719,#6719,#5535,.T.) ;
#8467=EDGE_CURVE('',#6719,#6720,#1818,.T.) ;
#8468=EDGE_CURVE('',#6720,#6720,#5536,.T.) ;
#8469=EDGE_CURVE('',#6721,#6722,#1819,.T.) ;
#8470=EDGE_CURVE('',#6721,#6723,#1820,.T.) ;
#8471=EDGE_CURVE('',#6724,#6723,#1821,.T.) ;
#8472=EDGE_CURVE('',#6724,#6722,#1822,.T.) ;
#8473=EDGE_CURVE('',#6725,#6726,#1823,.T.) ;
#8474=EDGE_CURVE('',#6725,#6727,#1824,.T.) ;
#8475=EDGE_CURVE('',#6728,#6727,#1825,.T.) ;
#8476=EDGE_CURVE('',#6728,#6726,#1826,.T.) ;
#8477=EDGE_CURVE('',#6729,#6721,#1827,.T.) ;
#8478=EDGE_CURVE('',#6727,#6729,#1828,.T.) ;
#8479=EDGE_CURVE('',#6730,#6725,#1829,.T.) ;
#8480=EDGE_CURVE('',#6723,#6730,#1830,.T.) ;
#8481=EDGE_CURVE('',#6729,#6731,#1831,.T.) ;
#8482=EDGE_CURVE('',#6722,#6731,#1832,.T.) ;
#8483=EDGE_CURVE('',#6730,#6732,#1833,.T.) ;
#8484=EDGE_CURVE('',#6726,#6732,#1834,.T.) ;
#8485=EDGE_CURVE('',#6731,#6728,#1835,.T.) ;
#8486=EDGE_CURVE('',#6732,#6724,#1836,.T.) ;
#11953=ORIENTED_EDGE('',*,*,#8466,.F.) ;
#11954=ORIENTED_EDGE('',*,*,#8467,.T.) ;
#11955=ORIENTED_EDGE('',*,*,#8468,.F.) ;
#11956=ORIENTED_EDGE('',*,*,#8467,.F.) ;
#11957=ORIENTED_EDGE('',*,*,#8469,.F.) ;
#11958=ORIENTED_EDGE('',*,*,#8470,.T.) ;
#11959=ORIENTED_EDGE('',*,*,#8471,.F.) ;
#11960=ORIENTED_EDGE('',*,*,#8472,.T.) ;
#11961=ORIENTED_EDGE('',*,*,#8473,.F.) ;
#11962=ORIENTED_EDGE('',*,*,#8474,.T.) ;
#11963=ORIENTED_EDGE('',*,*,#8475,.F.) ;
#11964=ORIENTED_EDGE('',*,*,#8476,.T.) ;
#11965=ORIENTED_EDGE('',*,*,#8470,.F.) ;
#11966=ORIENTED_EDGE('',*,*,#8477,.F.) ;
#11967=ORIENTED_EDGE('',*,*,#8478,.F.) ;
#11968=ORIENTED_EDGE('',*,*,#8474,.F.) ;
#11969=ORIENTED_EDGE('',*,*,#8479,.F.) ;
#11970=ORIENTED_EDGE('',*,*,#8480,.F.) ;
#11971=ORIENTED_EDGE('',*,*,#8466,.T.) ;
#11972=ORIENTED_EDGE('',*,*,#8481,.F.) ;
#11973=ORIENTED_EDGE('',*,*,#8477,.T.) ;
#11974=ORIENTED_EDGE('',*,*,#8469,.T.) ;
#11975=ORIENTED_EDGE('',*,*,#8482,.T.) ;
#11976=ORIENTED_EDGE('',*,*,#8483,.F.) ;
#11977=ORIENTED_EDGE('',*,*,#8479,.T.) ;
#11978=ORIENTED_EDGE('',*,*,#8473,.T.) ;
#11979=ORIENTED_EDGE('',*,*,#8484,.T.) ;
#11980=ORIENTED_EDGE('',*,*,#8481,.T.) ;
#11981=ORIENTED_EDGE('',*,*,#8485,.T.) ;
#11982=ORIENTED_EDGE('',*,*,#8475,.T.) ;
#11983=ORIENTED_EDGE('',*,*,#8478,.T.) ;
#11984=ORIENTED_EDGE('',*,*,#8471,.T.) ;
#11985=ORIENTED_EDGE('',*,*,#8480,.T.) ;
#11986=ORIENTED_EDGE('',*,*,#8483,.T.) ;
#11987=ORIENTED_EDGE('',*,*,#8486,.T.) ;
#11988=ORIENTED_EDGE('',*,*,#8472,.F.) ;
#11989=ORIENTED_EDGE('',*,*,#8486,.F.) ;
#11990=ORIENTED_EDGE('',*,*,#8484,.F.) ;
#11991=ORIENTED_EDGE('',*,*,#8476,.F.) ;
#11992=ORIENTED_EDGE('',*,*,#8485,.F.) ;
#11993=ORIENTED_EDGE('',*,*,#8482,.F.) ;
#11994=ORIENTED_EDGE('',*,*,#8468,.T.) ;
#12339=PLANE('',#15359) ;
#12340=PLANE('',#15360) ;
#12341=PLANE('',#15361) ;
#12342=PLANE('',#15362) ;
#12343=PLANE('',#15363) ;
#12344=PLANE('',#15364) ;
#12345=PLANE('',#15365) ;
#12346=PLANE('',#15366) ;
#13105=ADVANCED_FACE('',(#3710),#2951,.F.) ;
#13106=ADVANCED_FACE('',(#3711),#12339,.F.) ;
#13107=ADVANCED_FACE('',(#3712),#12340,.F.) ;
#13108=ADVANCED_FACE('',(#3713,#949),#12341,.T.) ;
#13109=ADVANCED_FACE('',(#3714),#12342,.F.) ;
#13110=ADVANCED_FACE('',(#3715),#12343,.F.) ;
#13111=ADVANCED_FACE('',(#3716),#12344,.F.) ;
#13112=ADVANCED_FACE('',(#3717),#12345,.F.) ;
#13113=ADVANCED_FACE('',(#3718,#950),#12346,.T.) ;
#13188=CLOSED_SHELL('',(#13105,#13106,#13107,#13108,#13109,#13110,#13111,
#13112,#13113)) ;
#15355=AXIS2_PLACEMENT_3D('',#24465,#19613,#19614) ;
#15356=AXIS2_PLACEMENT_3D('',#24466,#19615,#19616) ;
#15357=AXIS2_PLACEMENT_3D('',#24468,#19617,#19618) ;
#15358=AXIS2_PLACEMENT_3D('',#24471,#19620,#19621) ;
#15359=AXIS2_PLACEMENT_3D('',#24472,#19622,#19623) ;
#15360=AXIS2_PLACEMENT_3D('',#24481,#19628,#19629) ;
#15361=AXIS2_PLACEMENT_3D('',#24490,#19634,#19635) ;
#15362=AXIS2_PLACEMENT_3D('',#24497,#19640,#19641) ;
#15363=AXIS2_PLACEMENT_3D('',#24501,#19644,#19645) ;
#15364=AXIS2_PLACEMENT_3D('',#24505,#19648,#19649) ;
#15365=AXIS2_PLACEMENT_3D('',#24507,#19651,#19652) ;
#15366=AXIS2_PLACEMENT_3D('',#24509,#19654,#19655) ;
#19613=DIRECTION('axis',(0.,0.,1.)) ;
#19614=DIRECTION('refdir',(1.,0.,0.)) ;
#19615=DIRECTION('center_axis',(0.,1.,0.)) ;
#19616=DIRECTION('ref_axis',(1.,0.,0.)) ;
#19617=DIRECTION('center_axis',(0.,1.,0.)) ;
#19618=DIRECTION('ref_axis',(1.,0.,0.)) ;
#19619=DIRECTION('',(0.,1.,0.)) ;
#19620=DIRECTION('center_axis',(0.,-1.,0.)) ;
#19621=DIRECTION('ref_axis',(1.,0.,0.)) ;
#19622=DIRECTION('center_axis',(-0.5,0.,-0.866025403784439)) ;
#19623=DIRECTION('ref_axis',(-0.866025403784439,0.,0.5)) ;
#19624=DIRECTION('',(0.,1.,0.)) ;
#19625=DIRECTION('',(0.866025403784439,0.,-0.5)) ;
#19626=DIRECTION('',(0.,-1.,0.)) ;
#19627=DIRECTION('',(-0.866025403784439,0.,0.5)) ;
#19628=DIRECTION('center_axis',(0.5,0.,0.866025403784439)) ;
#19629=DIRECTION('ref_axis',(0.866025403784439,0.,-0.5)) ;
#19630=DIRECTION('',(0.,1.,0.)) ;
#19631=DIRECTION('',(-0.866025403784439,0.,0.5)) ;
#19632=DIRECTION('',(0.,-1.,0.)) ;
#19633=DIRECTION('',(0.866025403784439,0.,-0.5)) ;
#19634=DIRECTION('center_axis',(0.,-1.,0.)) ;
#19635=DIRECTION('ref_axis',(-1.,0.,0.)) ;
#19636=DIRECTION('',(0.866025403784439,0.,0.5)) ;
#19637=DIRECTION('',(0.,0.,1.)) ;
#19638=DIRECTION('',(-0.866025403784439,0.,-0.5)) ;
#19639=DIRECTION('',(0.,0.,-1.)) ;
#19640=DIRECTION('center_axis',(0.5,0.,-0.866025403784439)) ;
#19641=DIRECTION('ref_axis',(-0.866025403784439,0.,-0.5)) ;
#19642=DIRECTION('',(0.,1.,0.)) ;
#19643=DIRECTION('',(-0.866025403784439,0.,-0.5)) ;
#19644=DIRECTION('center_axis',(-0.5,0.,0.866025403784439)) ;
#19645=DIRECTION('ref_axis',(0.866025403784439,0.,0.5)) ;
#19646=DIRECTION('',(0.,1.,0.)) ;
#19647=DIRECTION('',(0.866025403784439,0.,0.5)) ;
#19648=DIRECTION('center_axis',(1.,0.,0.)) ;
#19649=DIRECTION('ref_axis',(0.,0.,-1.)) ;
#19650=DIRECTION('',(0.,0.,-1.)) ;
#19651=DIRECTION('center_axis',(-1.,0.,0.)) ;
#19652=DIRECTION('ref_axis',(0.,0.,1.)) ;
#19653=DIRECTION('',(0.,0.,1.)) ;
#19654=DIRECTION('center_axis',(0.,1.,0.)) ;
#19655=DIRECTION('ref_axis',(1.,0.,0.)) ;
#24465=CARTESIAN_POINT('',(0.,0.,0.)) ;
#24466=CARTESIAN_POINT('Origin',(0.,0.,0.)) ;
#24467=CARTESIAN_POINT('',(-0.3,-0.25,3.67394039744206E-17)) ;
#24468=CARTESIAN_POINT('Origin',(0.,-0.25,0.)) ;
#24469=CARTESIAN_POINT('',(-0.3,0.25,-3.67394039744206E-17)) ;
#24470=CARTESIAN_POINT('',(-0.3,0.,3.67394039744206E-17)) ;
#24471=CARTESIAN_POINT('Origin',(0.,0.25,0.)) ;
#24472=CARTESIAN_POINT('Origin',(0.25,0.,0.433012701892219)) ;
#24473=CARTESIAN_POINT('',(-8.32667268468867E-17,-0.25,0.577350269189626)) ;
#24474=CARTESIAN_POINT('',(-8.32667268468867E-17,0.25,0.577350269189626)) ;
#24475=CARTESIAN_POINT('',(-8.32667268468867E-17,0.,0.577350269189626)) ;
#24476=CARTESIAN_POINT('',(0.5,-0.25,0.288675134594813)) ;
#24477=CARTESIAN_POINT('',(0.25,-0.25,0.433012701892219)) ;
#24478=CARTESIAN_POINT('',(0.5,0.25,0.288675134594813)) ;
#24479=CARTESIAN_POINT('',(0.5,0.,0.288675134594813)) ;
#24480=CARTESIAN_POINT('',(0.25,0.25,0.433012701892219)) ;
#24481=CARTESIAN_POINT('Origin',(-0.25,0.,-0.433012701892219)) ;
#24482=CARTESIAN_POINT('',(8.32667268468867E-17,-0.25,-0.577350269189626)) ;
#24483=CARTESIAN_POINT('',(8.32667268468867E-17,0.25,-0.577350269189626)) ;
#24484=CARTESIAN_POINT('',(8.32667268468867E-17,0.,-0.577350269189626)) ;
#24485=CARTESIAN_POINT('',(-0.5,-0.25,-0.288675134594813)) ;
#24486=CARTESIAN_POINT('',(-0.25,-0.25,-0.433012701892219)) ;
#24487=CARTESIAN_POINT('',(-0.5,0.25,-0.288675134594813)) ;
#24488=CARTESIAN_POINT('',(-0.5,0.,-0.288675134594813)) ;
#24489=CARTESIAN_POINT('',(-0.25,0.25,-0.433012701892219)) ;
#24490=CARTESIAN_POINT('Origin',(0.,-0.25,0.)) ;
#24491=CARTESIAN_POINT('',(-0.5,-0.25,0.288675134594813)) ;
#24492=CARTESIAN_POINT('',(-0.25,-0.25,0.433012701892219)) ;
#24493=CARTESIAN_POINT('',(-0.5,-0.25,0.)) ;
#24494=CARTESIAN_POINT('',(0.5,-0.25,-0.288675134594813)) ;
#24495=CARTESIAN_POINT('',(0.25,-0.25,-0.433012701892219)) ;
#24496=CARTESIAN_POINT('',(0.5,-0.25,0.)) ;
#24497=CARTESIAN_POINT('Origin',(-0.25,0.,0.433012701892219)) ;
#24498=CARTESIAN_POINT('',(-0.5,0.25,0.288675134594813)) ;
#24499=CARTESIAN_POINT('',(-0.5,0.,0.288675134594813)) ;
#24500=CARTESIAN_POINT('',(-0.25,0.25,0.433012701892219)) ;
#24501=CARTESIAN_POINT('Origin',(0.25,0.,-0.433012701892219)) ;
#24502=CARTESIAN_POINT('',(0.5,0.25,-0.288675134594813)) ;
#24503=CARTESIAN_POINT('',(0.5,0.,-0.288675134594813)) ;
#24504=CARTESIAN_POINT('',(0.25,0.25,-0.433012701892219)) ;
#24505=CARTESIAN_POINT('Origin',(-0.5,0.,0.)) ;
#24506=CARTESIAN_POINT('',(-0.5,0.25,0.)) ;
#24507=CARTESIAN_POINT('Origin',(0.5,0.,0.)) ;
#24508=CARTESIAN_POINT('',(0.5,0.25,0.)) ;
#24509=CARTESIAN_POINT('Origin',(0.,0.25,0.)) ;
#24579=UNCERTAINTY_MEASURE_WITH_UNIT(LENGTH_MEASURE(0.001),#24629,
'DISTANCE_ACCURACY_VALUE',
'Maximum model space distance between geometric entities at asserted c
onnectivities') ;
#24580=UNCERTAINTY_MEASURE_WITH_UNIT(LENGTH_MEASURE(0.001),#24629,
'DISTANCE_ACCURACY_VALUE',
'Maximum model space distance between geometric entities at asserted c
onnectivities') ;
#24627=(
GEOMETRIC_REPRESENTATION_CONTEXT(3)
GLOBAL_UNCERTAINTY_ASSIGNED_CONTEXT((#24579))
GLOBAL_UNIT_ASSIGNED_CONTEXT((#24629,#24631,#24632))
REPRESENTATION_CONTEXT('','3D')
) ;
#24628=(
GEOMETRIC_REPRESENTATION_CONTEXT(3)
GLOBAL_UNCERTAINTY_ASSIGNED_CONTEXT((#24580))
GLOBAL_UNIT_ASSIGNED_CONTEXT((#24629,#24631,#24632))
REPRESENTATION_CONTEXT('','3D')
) ;
#24629=(
LENGTH_UNIT()
NAMED_UNIT(*)
SI_UNIT(.CENTI.,.METRE.)
) ;
#24631=(
NAMED_UNIT(*)
PLANE_ANGLE_UNIT()
SI_UNIT($,.RADIAN.)
) ;
#24632=(
NAMED_UNIT(*)
SI_UNIT($,.STERADIAN.)
SOLID_ANGLE_UNIT()
) ;
#24679=SHAPE_DEFINITION_REPRESENTATION(#24767,#24837) ;
#24767=PRODUCT_DEFINITION_SHAPE('',$,#24885) ;
#24837=SHAPE_REPRESENTATION('',(#15355),#24627) ;
#24838=PRODUCT_DEFINITION_CONTEXT('part definition',#24981,'design') ;
#24885=PRODUCT_DEFINITION('SHELL_CLAMP_NUT_M6',
'SHELL_CLAMP_NUT_M6',#24932,#24838) ;
#24932=PRODUCT_DEFINITION_FORMATION('',$,#25029) ;
#24981=APPLICATION_CONTEXT(
'Core Data for Automotive Mechanical Design Process') ;
#24982=PRODUCT_CONTEXT('part definition',#24981,'mechanical') ;
#25029=PRODUCT('SHELL_CLAMP_NUT_M6','SHELL_CLAMP_NUT_M6',$,(#24982)) ;
#25030=PRESENTATION_STYLE_ASSIGNMENT((#25040)) ;
#25040=SURFACE_STYLE_USAGE(.BOTH.,#25050) ;
#25050=SURFACE_SIDE_STYLE('',(#25060)) ;
#25060=SURFACE_STYLE_FILL_AREA(#25070) ;
#25070=FILL_AREA_STYLE('Steel - Satin',(#25080)) ;
#25080=FILL_AREA_STYLE_COLOUR('Steel - Satin',#25090) ;
#25090=COLOUR_RGB('Steel - Satin', 0.66274510, 0.83137255, 0.94901961) ;
ENDSEC;
END-ISO-10303-21;
